ISO-10303-21;
HEADER;
/* Generated by software containing ST-Developer
 * from STEP Tools, Inc. (www.steptools.com) 
 */
/* OPTION: using custom renumber hook */

FILE_DESCRIPTION(
/* description */ ('STEP AP242 Edition 2', 'CAx-IF Rec.Pracs.---Representation and Presentation of Product Manufa
cturing Information (PMI)---4.0---2014-10-13', 'CAx-IF Rec.Pracs.---3D Tessellated Geometry---0.4---2014-09-14', '2;1', 'CAx-IF Rec.Pracs.---User Defined Attributes---1.5---2016-08-15'),
/* implementation_level */ '2;1');

FILE_NAME(
/* name */ 'main_housing.step',
/* time_stamp */ '2026-10-08T12:15:07Z',
/* author */ (''),
/* organization */ (''),
/* preprocessor_version */ 'ST-DEVELOPER v20',
/* originating_system */ 'ONSHAPE BY PTC INC, 1.221',
/* authorisation */ '  ');

FILE_SCHEMA (('AP242_MANAGED_MODEL_BASED_3D_ENGINEERING_MIM_LF { 1 0 10303 442 3 1 4 }'));
ENDSEC;

DATA;
#26=CONICAL_SURFACE('',#14356,0.00512938524157182,1.22173047639604);
#27=CONICAL_SURFACE('',#14358,0.00325,0.610865238198018);
#28=CONICAL_SURFACE('',#14363,0.00312938524157182,0.610865238198019);
#29=CONICAL_SURFACE('',#14366,0.008,1.22173047639604);
#60=COLOUR_RGB('', 0.66274510, 0.83137255, 0.94901961);
#211=SHAPE_REPRESENTATION_RELATIONSHIP('','',#13785,#238);
#238=ADVANCED_BREP_SHAPE_REPRESENTATION('',(#13729),#45475);
#307=TOROIDAL_SURFACE('',#14354,0.009,0.003);
#308=TOROIDAL_SURFACE('',#14369,0.00696039327083855,0.00303960672916145);
#309=TOROIDAL_SURFACE('',#14373,0.013,0.001);
#310=TOROIDAL_SURFACE('',#14374,0.0187,0.0002);
#311=TOROIDAL_SURFACE('',#14375,0.0118,0.0002);
#312=TOROIDAL_SURFACE('',#14376,0.0102,0.0002);
#313=TOROIDAL_SURFACE('',#14377,0.0037676893301498,0.001);
#314=TOROIDAL_SURFACE('',#14378,0.00225,0.001);
#621=CIRCLE('',#14336,0.00125);
#622=CIRCLE('',#14337,0.00325);
#623=CIRCLE('',#14339,0.012);
#624=CIRCLE('',#14340,0.0189);
#625=CIRCLE('',#14342,0.013);
#626=CIRCLE('',#14343,0.0187);
#627=CIRCLE('',#14345,0.0102);
#628=CIRCLE('',#14346,0.0118);
#629=CIRCLE('',#14348,0.012);
#630=CIRCLE('',#14349,0.012);
#631=CIRCLE('',#14351,0.0189);
#632=CIRCLE('',#14353,0.012);
#633=CIRCLE('',#14355,0.010026060429977);
#634=CIRCLE('',#14357,0.00512938524157182);
#635=CIRCLE('',#14359,0.00325);
#636=CIRCLE('',#14362,0.00125);
#637=CIRCLE('',#14364,0.00294853728586081);
#638=CIRCLE('',#14365,0.00143084795571101);
#639=CIRCLE('',#14367,0.008);
#640=CIRCLE('',#14368,0.00342566918682414);
#641=CIRCLE('',#14370,0.01);
#642=CIRCLE('',#14372,0.01);
#1286=PLANE('',#14335);
#1287=PLANE('',#14338);
#1288=PLANE('',#14341);
#1289=PLANE('',#14344);
#1631=CYLINDRICAL_SURFACE('',#14347,0.012);
#1632=CYLINDRICAL_SURFACE('',#14350,0.0189);
#1633=CYLINDRICAL_SURFACE('',#14352,0.012);
#1634=CYLINDRICAL_SURFACE('',#14360,0.00325);
#1635=CYLINDRICAL_SURFACE('',#14361,0.00125);
#1636=CYLINDRICAL_SURFACE('',#14371,0.01);
#3024=ORIENTED_EDGE('',*,*,#6159,.F.);
#3025=ORIENTED_EDGE('',*,*,#6160,.T.);
#3026=ORIENTED_EDGE('',*,*,#6161,.F.);
#3027=ORIENTED_EDGE('',*,*,#6162,.T.);
#3028=ORIENTED_EDGE('',*,*,#6163,.T.);
#3029=ORIENTED_EDGE('',*,*,#6164,.T.);
#3030=ORIENTED_EDGE('',*,*,#6165,.T.);
#3031=ORIENTED_EDGE('',*,*,#6166,.T.);
#3032=ORIENTED_EDGE('',*,*,#6167,.T.);
#3033=ORIENTED_EDGE('',*,*,#6168,.T.);
#3034=ORIENTED_EDGE('',*,*,#6162,.F.);
#3035=ORIENTED_EDGE('',*,*,#6169,.T.);
#3036=ORIENTED_EDGE('',*,*,#6170,.F.);
#3037=ORIENTED_EDGE('',*,*,#6161,.T.);
#3038=ORIENTED_EDGE('',*,*,#6171,.F.);
#3039=ORIENTED_EDGE('',*,*,#6170,.T.);
#3040=ORIENTED_EDGE('',*,*,#6171,.T.);
#3041=ORIENTED_EDGE('',*,*,#6172,.F.);
#3042=ORIENTED_EDGE('',*,*,#6172,.T.);
#3043=ORIENTED_EDGE('',*,*,#6173,.F.);
#3044=ORIENTED_EDGE('',*,*,#6160,.F.);
#3045=ORIENTED_EDGE('',*,*,#6173,.T.);
#3046=ORIENTED_EDGE('',*,*,#6159,.T.);
#3047=ORIENTED_EDGE('',*,*,#6174,.T.);
#3048=ORIENTED_EDGE('',*,*,#6175,.T.);
#3049=ORIENTED_EDGE('',*,*,#6176,.T.);
#3050=ORIENTED_EDGE('',*,*,#6177,.F.);
#3051=ORIENTED_EDGE('',*,*,#6178,.T.);
#3052=ORIENTED_EDGE('',*,*,#6177,.T.);
#3053=ORIENTED_EDGE('',*,*,#6179,.F.);
#3054=ORIENTED_EDGE('',*,*,#6179,.T.);
#3055=ORIENTED_EDGE('',*,*,#6180,.T.);
#3056=ORIENTED_EDGE('',*,*,#6163,.F.);
#3057=ORIENTED_EDGE('',*,*,#6167,.F.);
#3058=ORIENTED_EDGE('',*,*,#6164,.F.);
#3059=ORIENTED_EDGE('',*,*,#6169,.F.);
#3060=ORIENTED_EDGE('',*,*,#6166,.F.);
#3061=ORIENTED_EDGE('',*,*,#6168,.F.);
#3062=ORIENTED_EDGE('',*,*,#6180,.F.);
#3063=ORIENTED_EDGE('',*,*,#6165,.F.);
#3064=ORIENTED_EDGE('',*,*,#6175,.F.);
#3065=ORIENTED_EDGE('',*,*,#6178,.F.);
#3066=ORIENTED_EDGE('',*,*,#6174,.F.);
#3067=ORIENTED_EDGE('',*,*,#6176,.F.);
#6159=EDGE_CURVE('',#7845,#7845,#621,.T.);
#6160=EDGE_CURVE('',#7846,#7846,#622,.T.);
#6161=EDGE_CURVE('',#7847,#7847,#623,.T.);
#6162=EDGE_CURVE('',#7848,#7848,#624,.T.);
#6163=EDGE_CURVE('',#7849,#7849,#625,.T.);
#6164=EDGE_CURVE('',#7850,#7850,#626,.T.);
#6165=EDGE_CURVE('',#7851,#7851,#627,.T.);
#6166=EDGE_CURVE('',#7852,#7852,#628,.T.);
#6167=EDGE_CURVE('',#7853,#7853,#629,.T.);
#6168=EDGE_CURVE('',#7854,#7854,#630,.T.);
#6169=EDGE_CURVE('',#7855,#7855,#631,.T.);
#6170=EDGE_CURVE('',#7856,#7856,#632,.T.);
#6171=EDGE_CURVE('',#7857,#7857,#633,.T.);
#6172=EDGE_CURVE('',#7858,#7858,#634,.T.);
#6173=EDGE_CURVE('',#7859,#7859,#635,.T.);
#6174=EDGE_CURVE('',#7860,#7860,#636,.T.);
#6175=EDGE_CURVE('',#7861,#7861,#637,.T.);
#6176=EDGE_CURVE('',#7862,#7862,#638,.T.);
#6177=EDGE_CURVE('',#7863,#7863,#639,.T.);
#6178=EDGE_CURVE('',#7864,#7864,#640,.T.);
#6179=EDGE_CURVE('',#7865,#7865,#641,.T.);
#6180=EDGE_CURVE('',#7866,#7866,#642,.T.);
#7845=VERTEX_POINT('',#33498);
#7846=VERTEX_POINT('',#33500);
#7847=VERTEX_POINT('',#33503);
#7848=VERTEX_POINT('',#33505);
#7849=VERTEX_POINT('',#33508);
#7850=VERTEX_POINT('',#33510);
#7851=VERTEX_POINT('',#33513);
#7852=VERTEX_POINT('',#33515);
#7853=VERTEX_POINT('',#33518);
#7854=VERTEX_POINT('',#33520);
#7855=VERTEX_POINT('',#33523);
#7856=VERTEX_POINT('',#33526);
#7857=VERTEX_POINT('',#33529);
#7858=VERTEX_POINT('',#33532);
#7859=VERTEX_POINT('',#33535);
#7860=VERTEX_POINT('',#33539);
#7861=VERTEX_POINT('',#33542);
#7862=VERTEX_POINT('',#33544);
#7863=VERTEX_POINT('',#33547);
#7864=VERTEX_POINT('',#33549);
#7865=VERTEX_POINT('',#33552);
#7866=VERTEX_POINT('',#33555);
#10843=EDGE_LOOP('',(#3024));
#10844=EDGE_LOOP('',(#3025));
#10845=EDGE_LOOP('',(#3026));
#10846=EDGE_LOOP('',(#3027));
#10847=EDGE_LOOP('',(#3028));
#10848=EDGE_LOOP('',(#3029));
#10849=EDGE_LOOP('',(#3030));
#10850=EDGE_LOOP('',(#3031));
#10851=EDGE_LOOP('',(#3032));
#10852=EDGE_LOOP('',(#3033));
#10853=EDGE_LOOP('',(#3034));
#10854=EDGE_LOOP('',(#3035));
#10855=EDGE_LOOP('',(#3036));
#10856=EDGE_LOOP('',(#3037));
#10857=EDGE_LOOP('',(#3038));
#10858=EDGE_LOOP('',(#3039));
#10859=EDGE_LOOP('',(#3040));
#10860=EDGE_LOOP('',(#3041));
#10861=EDGE_LOOP('',(#3042));
#10862=EDGE_LOOP('',(#3043));
#10863=EDGE_LOOP('',(#3044));
#10864=EDGE_LOOP('',(#3045));
#10865=EDGE_LOOP('',(#3046));
#10866=EDGE_LOOP('',(#3047));
#10867=EDGE_LOOP('',(#3048));
#10868=EDGE_LOOP('',(#3049));
#10869=EDGE_LOOP('',(#3050));
#10870=EDGE_LOOP('',(#3051));
#10871=EDGE_LOOP('',(#3052));
#10872=EDGE_LOOP('',(#3053));
#10873=EDGE_LOOP('',(#3054));
#10874=EDGE_LOOP('',(#3055));
#10875=EDGE_LOOP('',(#3056));
#10876=EDGE_LOOP('',(#3057));
#10877=EDGE_LOOP('',(#3058));
#10878=EDGE_LOOP('',(#3059));
#10879=EDGE_LOOP('',(#3060));
#10880=EDGE_LOOP('',(#3061));
#10881=EDGE_LOOP('',(#3062));
#10882=EDGE_LOOP('',(#3063));
#10883=EDGE_LOOP('',(#3064));
#10884=EDGE_LOOP('',(#3065));
#10885=EDGE_LOOP('',(#3066));
#10886=EDGE_LOOP('',(#3067));
#11960=FACE_BOUND('',#10843,.T.);
#11961=FACE_BOUND('',#10844,.T.);
#11962=FACE_BOUND('',#10845,.T.);
#11963=FACE_BOUND('',#10846,.T.);
#11964=FACE_BOUND('',#10847,.T.);
#11965=FACE_BOUND('',#10848,.T.);
#11966=FACE_BOUND('',#10849,.T.);
#11967=FACE_BOUND('',#10850,.T.);
#11968=FACE_BOUND('',#10851,.T.);
#11969=FACE_BOUND('',#10852,.T.);
#11970=FACE_BOUND('',#10853,.T.);
#11971=FACE_BOUND('',#10854,.T.);
#11972=FACE_BOUND('',#10855,.T.);
#11973=FACE_BOUND('',#10856,.T.);
#11974=FACE_BOUND('',#10857,.T.);
#11975=FACE_BOUND('',#10858,.T.);
#11976=FACE_BOUND('',#10859,.T.);
#11977=FACE_BOUND('',#10860,.T.);
#11978=FACE_BOUND('',#10861,.T.);
#11979=FACE_BOUND('',#10862,.T.);
#11980=FACE_BOUND('',#10863,.T.);
#11981=FACE_BOUND('',#10864,.T.);
#11982=FACE_BOUND('',#10865,.T.);
#11983=FACE_BOUND('',#10866,.T.);
#11984=FACE_BOUND('',#10867,.T.);
#11985=FACE_BOUND('',#10868,.T.);
#11986=FACE_BOUND('',#10869,.T.);
#11987=FACE_BOUND('',#10870,.T.);
#11988=FACE_BOUND('',#10871,.T.);
#11989=FACE_BOUND('',#10872,.T.);
#11990=FACE_BOUND('',#10873,.T.);
#11991=FACE_BOUND('',#10874,.T.);
#11992=FACE_BOUND('',#10875,.T.);
#11993=FACE_BOUND('',#10876,.T.);
#11994=FACE_BOUND('',#10877,.T.);
#11995=FACE_BOUND('',#10878,.T.);
#11996=FACE_BOUND('',#10879,.T.);
#11997=FACE_BOUND('',#10880,.T.);
#11998=FACE_BOUND('',#10881,.T.);
#11999=FACE_BOUND('',#10882,.T.);
#12000=FACE_BOUND('',#10883,.T.);
#12001=FACE_BOUND('',#10884,.T.);
#12002=FACE_BOUND('',#10885,.T.);
#12003=FACE_BOUND('',#10886,.T.);
#12978=ADVANCED_FACE('',(#11960,#11961),#1286,.T.);
#12979=ADVANCED_FACE('',(#11962,#11963),#1287,.T.);
#12980=ADVANCED_FACE('',(#11964,#11965),#1288,.T.);
#12981=ADVANCED_FACE('',(#11966,#11967),#1289,.T.);
#12982=ADVANCED_FACE('',(#11968,#11969),#1631,.T.);
#12983=ADVANCED_FACE('',(#11970,#11971),#1632,.T.);
#12984=ADVANCED_FACE('',(#11972,#11973),#1633,.T.);
#12985=ADVANCED_FACE('',(#11974,#11975),#307,.T.);
#12986=ADVANCED_FACE('',(#11976,#11977),#26,.T.);
#12987=ADVANCED_FACE('',(#11978,#11979),#27,.T.);
#12988=ADVANCED_FACE('',(#11980,#11981),#1634,.T.);
#12989=ADVANCED_FACE('',(#11982,#11983),#1635,.F.);
#12990=ADVANCED_FACE('',(#11984,#11985),#28,.F.);
#12991=ADVANCED_FACE('',(#11986,#11987),#29,.F.);
#12992=ADVANCED_FACE('',(#11988,#11989),#308,.F.);
#12993=ADVANCED_FACE('',(#11990,#11991),#1636,.F.);
#12994=ADVANCED_FACE('',(#11992,#11993),#309,.F.);
#12995=ADVANCED_FACE('',(#11994,#11995),#310,.T.);
#12996=ADVANCED_FACE('',(#11996,#11997),#311,.T.);
#12997=ADVANCED_FACE('',(#11998,#11999),#312,.T.);
#12998=ADVANCED_FACE('',(#12000,#12001),#313,.T.);
#12999=ADVANCED_FACE('',(#12002,#12003),#314,.T.);
#13512=CLOSED_SHELL('',(#12978,#12979,#12980,#12981,#12982,#12983,#12984,
#12985,#12986,#12987,#12988,#12989,#12990,#12991,#12992,#12993,#12994,#12995,
#12996,#12997,#12998,#12999));
#13539=STYLED_ITEM('',(#13566),#13729);
#13566=PRESENTATION_STYLE_ASSIGNMENT((#13593));
#13593=SURFACE_STYLE_USAGE(.BOTH.,#13620);
#13620=SURFACE_SIDE_STYLE('',(#13647));
#13647=SURFACE_STYLE_FILL_AREA(#13674);
#13674=FILL_AREA_STYLE('',(#13701));
#13701=FILL_AREA_STYLE_COLOUR('',#60);
#13729=MANIFOLD_SOLID_BREP('main_housing',#13512);
#13757=SHAPE_DEFINITION_REPRESENTATION(#45546,#13785);
#13785=SHAPE_REPRESENTATION('main_housing',(#13802),#45475);
#13802=AXIS2_PLACEMENT_3D('',#19109,#15295,#15296);
#14335=AXIS2_PLACEMENT_3D('',#33496,#16491,#16492);
#14336=AXIS2_PLACEMENT_3D('',#33497,#16493,#16494);
#14337=AXIS2_PLACEMENT_3D('',#33499,#16495,#16496);
#14338=AXIS2_PLACEMENT_3D('',#33501,#16497,#16498);
#14339=AXIS2_PLACEMENT_3D('',#33502,#16499,#16500);
#14340=AXIS2_PLACEMENT_3D('',#33504,#16501,#16502);
#14341=AXIS2_PLACEMENT_3D('',#33506,#16503,#16504);
#14342=AXIS2_PLACEMENT_3D('',#33507,#16505,#16506);
#14343=AXIS2_PLACEMENT_3D('',#33509,#16507,#16508);
#14344=AXIS2_PLACEMENT_3D('',#33511,#16509,#16510);
#14345=AXIS2_PLACEMENT_3D('',#33512,#16511,#16512);
#14346=AXIS2_PLACEMENT_3D('',#33514,#16513,#16514);
#14347=AXIS2_PLACEMENT_3D('',#33516,#16515,#16516);
#14348=AXIS2_PLACEMENT_3D('',#33517,#16517,#16518);
#14349=AXIS2_PLACEMENT_3D('',#33519,#16519,#16520);
#14350=AXIS2_PLACEMENT_3D('',#33521,#16521,#16522);
#14351=AXIS2_PLACEMENT_3D('',#33522,#16523,#16524);
#14352=AXIS2_PLACEMENT_3D('',#33524,#16525,#16526);
#14353=AXIS2_PLACEMENT_3D('',#33525,#16527,#16528);
#14354=AXIS2_PLACEMENT_3D('',#33527,#16529,#16530);
#14355=AXIS2_PLACEMENT_3D('',#33528,#16531,#16532);
#14356=AXIS2_PLACEMENT_3D('',#33530,#16533,#16534);
#14357=AXIS2_PLACEMENT_3D('',#33531,#16535,#16536);
#14358=AXIS2_PLACEMENT_3D('',#33533,#16537,#16538);
#14359=AXIS2_PLACEMENT_3D('',#33534,#16539,#16540);
#14360=AXIS2_PLACEMENT_3D('',#33536,#16541,#16542);
#14361=AXIS2_PLACEMENT_3D('',#33537,#16543,#16544);
#14362=AXIS2_PLACEMENT_3D('',#33538,#16545,#16546);
#14363=AXIS2_PLACEMENT_3D('',#33540,#16547,#16548);
#14364=AXIS2_PLACEMENT_3D('',#33541,#16549,#16550);
#14365=AXIS2_PLACEMENT_3D('',#33543,#16551,#16552);
#14366=AXIS2_PLACEMENT_3D('',#33545,#16553,#16554);
#14367=AXIS2_PLACEMENT_3D('',#33546,#16555,#16556);
#14368=AXIS2_PLACEMENT_3D('',#33548,#16557,#16558);
#14369=AXIS2_PLACEMENT_3D('',#33550,#16559,#16560);
#14370=AXIS2_PLACEMENT_3D('',#33551,#16561,#16562);
#14371=AXIS2_PLACEMENT_3D('',#33553,#16563,#16564);
#14372=AXIS2_PLACEMENT_3D('',#33554,#16565,#16566);
#14373=AXIS2_PLACEMENT_3D('',#33556,#16567,#16568);
#14374=AXIS2_PLACEMENT_3D('',#33557,#16569,#16570);
#14375=AXIS2_PLACEMENT_3D('',#33558,#16571,#16572);
#14376=AXIS2_PLACEMENT_3D('',#33559,#16573,#16574);
#14377=AXIS2_PLACEMENT_3D('',#33560,#16575,#16576);
#14378=AXIS2_PLACEMENT_3D('',#33561,#16577,#16578);
#15295=DIRECTION('',(0.,0.,1.));
#15296=DIRECTION('',(1.,0.,0.));
#16491=DIRECTION('',(0.,0.,-1.));
#16492=DIRECTION('',(-1.,0.,0.));
#16493=DIRECTION('',(0.,0.,-1.));
#16494=DIRECTION('',(-1.,0.,0.));
#16495=DIRECTION('',(0.,0.,-1.));
#16496=DIRECTION('',(-1.,0.,0.));
#16497=DIRECTION('',(0.,0.,-1.));
#16498=DIRECTION('',(-1.,0.,0.));
#16499=DIRECTION('',(0.,0.,-1.));
#16500=DIRECTION('',(-1.,0.,0.));
#16501=DIRECTION('',(0.,0.,-1.));
#16502=DIRECTION('',(-1.,0.,0.));
#16503=DIRECTION('',(0.,0.,1.));
#16504=DIRECTION('',(1.,0.,0.));
#16505=DIRECTION('',(0.,0.,-1.));
#16506=DIRECTION('',(1.,0.,0.));
#16507=DIRECTION('',(0.,0.,1.));
#16508=DIRECTION('',(1.,0.,0.));
#16509=DIRECTION('',(0.,0.,1.));
#16510=DIRECTION('',(1.,0.,0.));
#16511=DIRECTION('',(0.,0.,-1.));
#16512=DIRECTION('',(1.,0.,0.));
#16513=DIRECTION('',(0.,0.,1.));
#16514=DIRECTION('',(1.,0.,0.));
#16515=DIRECTION('',(0.,0.,-1.));
#16516=DIRECTION('',(-1.,0.,0.));
#16517=DIRECTION('',(0.,0.,1.));
#16518=DIRECTION('',(1.,0.,0.));
#16519=DIRECTION('',(0.,0.,-1.));
#16520=DIRECTION('',(1.,0.,0.));
#16521=DIRECTION('',(0.,0.,-1.));
#16522=DIRECTION('',(-1.,0.,0.));
#16523=DIRECTION('',(0.,0.,-1.));
#16524=DIRECTION('',(1.,0.,0.));
#16525=DIRECTION('',(0.,0.,-1.));
#16526=DIRECTION('',(-1.,0.,0.));
#16527=DIRECTION('',(0.,0.,-1.));
#16528=DIRECTION('',(-1.,0.,0.));
#16529=DIRECTION('',(0.,0.,-1.));
#16530=DIRECTION('',(-1.,0.,0.));
#16531=DIRECTION('',(0.,0.,-1.));
#16532=DIRECTION('',(-1.,0.,0.));
#16533=DIRECTION('',(0.,0.,1.));
#16534=DIRECTION('',(1.,0.,0.));
#16535=DIRECTION('',(0.,0.,-1.));
#16536=DIRECTION('',(-1.,0.,0.));
#16537=DIRECTION('',(0.,0.,1.));
#16538=DIRECTION('',(1.,0.,0.));
#16539=DIRECTION('',(0.,0.,-1.));
#16540=DIRECTION('',(-1.,0.,0.));
#16541=DIRECTION('',(0.,0.,-1.));
#16542=DIRECTION('',(-1.,0.,0.));
#16543=DIRECTION('',(0.,0.,-1.));
#16544=DIRECTION('',(-1.,0.,0.));
#16545=DIRECTION('',(0.,0.,1.));
#16546=DIRECTION('',(1.,0.,0.));
#16547=DIRECTION('',(0.,0.,1.));
#16548=DIRECTION('',(1.,0.,0.));
#16549=DIRECTION('',(0.,0.,1.));
#16550=DIRECTION('',(-1.,0.,0.));
#16551=DIRECTION('',(0.,0.,-1.));
#16552=DIRECTION('',(-1.,0.,0.));
#16553=DIRECTION('',(0.,0.,1.));
#16554=DIRECTION('',(1.,0.,0.));
#16555=DIRECTION('',(0.,0.,-1.));
#16556=DIRECTION('',(-1.,0.,0.));
#16557=DIRECTION('',(0.,0.,-1.));
#16558=DIRECTION('',(-1.,0.,0.));
#16559=DIRECTION('',(0.,0.,-1.));
#16560=DIRECTION('',(-1.,0.,0.));
#16561=DIRECTION('',(0.,0.,-1.));
#16562=DIRECTION('',(-1.,0.,0.));
#16563=DIRECTION('',(0.,0.,-1.));
#16564=DIRECTION('',(-1.,0.,0.));
#16565=DIRECTION('',(0.,0.,1.));
#16566=DIRECTION('',(1.,0.,0.));
#16567=DIRECTION('',(0.,0.,1.));
#16568=DIRECTION('',(1.,0.,0.));
#16569=DIRECTION('',(0.,0.,1.));
#16570=DIRECTION('',(1.,0.,0.));
#16571=DIRECTION('',(0.,0.,1.));
#16572=DIRECTION('',(1.,0.,0.));
#16573=DIRECTION('',(0.,0.,1.));
#16574=DIRECTION('',(1.,0.,0.));
#16575=DIRECTION('',(0.,0.,1.));
#16576=DIRECTION('',(1.,0.,0.));
#16577=DIRECTION('',(0.,0.,1.));
#16578=DIRECTION('',(1.,0.,0.));
#19109=CARTESIAN_POINT('',(0.,0.,0.));
#33496=CARTESIAN_POINT('',(-0.00125,0.,-0.0300923697749146));
#33497=CARTESIAN_POINT('',(0.,0.,-0.0300923697749146));
#33498=CARTESIAN_POINT('',(-0.00125,0.,-0.0300923697749146));
#33499=CARTESIAN_POINT('',(0.,0.,-0.0300923697749146));
#33500=CARTESIAN_POINT('',(-0.00325,0.,-0.0300923697749146));
#33501=CARTESIAN_POINT('',(-0.0189,0.,0.0230923697749146));
#33502=CARTESIAN_POINT('',(0.,0.,0.0230923697749146));
#33503=CARTESIAN_POINT('',(-0.012,0.,0.0230923697749146));
#33504=CARTESIAN_POINT('',(0.,0.,0.0230923697749146));
#33505=CARTESIAN_POINT('',(-0.0189,0.,0.0230923697749146));
#33506=CARTESIAN_POINT('',(-0.012,0.,0.0250923697749146));
#33507=CARTESIAN_POINT('',(0.,0.,0.0250923697749146));
#33508=CARTESIAN_POINT('',(0.013,0.,0.0250923697749146));
#33509=CARTESIAN_POINT('',(0.,0.,0.0250923697749146));
#33510=CARTESIAN_POINT('',(0.0187,0.,0.0250923697749146));
#33511=CARTESIAN_POINT('',(-0.012,0.,0.0300923697749146));
#33512=CARTESIAN_POINT('',(0.,0.,0.0300923697749146));
#33513=CARTESIAN_POINT('',(0.0102,0.,0.0300923697749146));
#33514=CARTESIAN_POINT('',(0.,0.,0.0300923697749146));
#33515=CARTESIAN_POINT('',(0.0118,0.,0.0300923697749146));
#33516=CARTESIAN_POINT('',(0.,0.,-0.0300923697749146));
#33517=CARTESIAN_POINT('',(0.,0.,0.0260923697749146));
#33518=CARTESIAN_POINT('',(0.012,0.,0.0260923697749146));
#33519=CARTESIAN_POINT('',(0.,0.,0.0298923697749146));
#33520=CARTESIAN_POINT('',(0.012,0.,0.0298923697749146));
#33521=CARTESIAN_POINT('',(0.,0.,-0.0300923697749146));
#33522=CARTESIAN_POINT('',(0.,0.,0.0248923697749146));
#33523=CARTESIAN_POINT('',(0.0189,0.,0.0248923697749146));
#33524=CARTESIAN_POINT('',(0.,0.,-0.0300923697749146));
#33525=CARTESIAN_POINT('',(0.,0.,-0.0162074226868757));
#33526=CARTESIAN_POINT('',(-0.012,0.,-0.0162074226868757));
#33527=CARTESIAN_POINT('',(0.,0.,-0.0162074226868757));
#33528=CARTESIAN_POINT('',(0.,0.,-0.0190265005492334));
#33529=CARTESIAN_POINT('',(-0.010026060429977,0.,-0.0190265005492334));
#33530=CARTESIAN_POINT('',(0.,0.,-0.0208087445646827));
#33531=CARTESIAN_POINT('',(0.,0.,-0.0208087445646827));
#33532=CARTESIAN_POINT('',(-0.00512938524157182,0.,-0.0208087445646827));
#33533=CARTESIAN_POINT('',(0.,0.,-0.0234927848513341));
#33534=CARTESIAN_POINT('',(0.,0.,-0.0234927848513341));
#33535=CARTESIAN_POINT('',(-0.00325,0.,-0.0234927848513341));
#33536=CARTESIAN_POINT('',(0.,0.,-0.0300923697749146));
#33537=CARTESIAN_POINT('',(0.,0.,-0.0300923697749146));
#33538=CARTESIAN_POINT('',(0.,0.,-0.0224076685637936));
#33539=CARTESIAN_POINT('',(0.00125,0.,-0.0224076685637936));
#33540=CARTESIAN_POINT('',(0.,0.,-0.0194083294882633));
#33541=CARTESIAN_POINT('',(0.,0.,-0.0196666071357353));
#33542=CARTESIAN_POINT('',(-0.00294853728586081,0.,-0.0196666071357353));
#33543=CARTESIAN_POINT('',(0.,0.,-0.0218340921274426));
#33544=CARTESIAN_POINT('',(-0.00143084795571101,0.,-0.0218340921274426));
#33545=CARTESIAN_POINT('',(0.,0.,-0.0176355706936178));
#33546=CARTESIAN_POINT('',(0.,0.,-0.0176355706936178));
#33547=CARTESIAN_POINT('',(-0.008,0.,-0.0176355706936178));
#33548=CARTESIAN_POINT('',(0.,0.,-0.0193004909513005));
#33549=CARTESIAN_POINT('',(-0.00342566918682414,0.,-0.0193004909513005));
#33550=CARTESIAN_POINT('',(0.,0.,-0.0147792746801336));
#33551=CARTESIAN_POINT('',(0.,0.,-0.0147792746801336));
#33552=CARTESIAN_POINT('',(-0.01,0.,-0.0147792746801336));
#33553=CARTESIAN_POINT('',(0.,0.,-0.0300923697749146));
#33554=CARTESIAN_POINT('',(0.,0.,0.0298923697749146));
#33555=CARTESIAN_POINT('',(0.01,0.,0.0298923697749146));
#33556=CARTESIAN_POINT('',(0.,0.,0.0260923697749146));
#33557=CARTESIAN_POINT('',(0.,0.,0.0248923697749146));
#33558=CARTESIAN_POINT('',(0.,0.,0.0298923697749146));
#33559=CARTESIAN_POINT('',(0.,0.,0.0298923697749146));
#33560=CARTESIAN_POINT('',(0.,0.,-0.0202401835720864));
#33561=CARTESIAN_POINT('',(0.,0.,-0.0224076685637936));
#45463=MECHANICAL_DESIGN_GEOMETRIC_PRESENTATION_REPRESENTATION('',(#13539),#45464);
#45464=(
GEOMETRIC_REPRESENTATION_CONTEXT(3)
GLOBAL_UNCERTAINTY_ASSIGNED_CONTEXT((#45492))
GLOBAL_UNIT_ASSIGNED_CONTEXT((#45522,#45521,#45520))
REPRESENTATION_CONTEXT('MAS-690','TOP_LEVEL_ASSEMBLY_PART')
);
#45475=(
GEOMETRIC_REPRESENTATION_CONTEXT(3)
GLOBAL_UNCERTAINTY_ASSIGNED_CONTEXT((#45503))
GLOBAL_UNIT_ASSIGNED_CONTEXT((#45522,#45521,#45520))
REPRESENTATION_CONTEXT('main_housing','COMPONENT_PART')
);
#45492=UNCERTAINTY_MEASURE_WITH_UNIT(LENGTH_MEASURE(1.E-8),#45522,
'DISTANCE_ACCURACY_VALUE','Maximum Tolerance applied to model');
#45503=UNCERTAINTY_MEASURE_WITH_UNIT(LENGTH_MEASURE(1.E-8),#45522,
'DISTANCE_ACCURACY_VALUE','Maximum Tolerance applied to model');
#45520=(
NAMED_UNIT(*)
SI_UNIT($,.STERADIAN.)
SOLID_ANGLE_UNIT()
);
#45521=(
NAMED_UNIT(*)
PLANE_ANGLE_UNIT()
SI_UNIT($,.RADIAN.)
);
#45522=(
LENGTH_UNIT()
NAMED_UNIT(*)
SI_UNIT($,.METRE.)
);
#45546=PRODUCT_DEFINITION_SHAPE('','',#45596);
#45596=PRODUCT_DEFINITION('','',#45652,#45624);
#45624=PRODUCT_DEFINITION_CONTEXT('',#45782,'design');
#45652=PRODUCT_DEFINITION_FORMATION_WITH_SPECIFIED_SOURCE('','',#45708,
 .NOT_KNOWN.);
#45708=PRODUCT('main_housing','main_housing','main_housing',(#45764));
#45764=PRODUCT_CONTEXT('',#45782,'mechanical');
#45782=APPLICATION_CONTEXT('managed model based 3d engineering');
ENDSEC;
END-ISO-10303-21;
